ISO-10303-21;
HEADER;
/* Generated by software containing ST-Developer
 * from STEP Tools, Inc. (www.steptools.com) 
 */

FILE_DESCRIPTION(
/* description */ ('Round-Shaft Linear Stage with Ball Bushings'),
/* implementation_level */ '2;1');

FILE_NAME(
/* name */ 'Cap Screw - M6x25.step',
/* time_stamp */ '2026-10-27T10:47:55-07:00',
/* author */ (''),
/* organization */ (''),
/* preprocessor_version */ 'ST-DEVELOPER v20.2',
/* originating_system */ 'Autodesk Translation Framework v15.17.0.0',
/* authorisation */ '');

FILE_SCHEMA (('AUTOMOTIVE_DESIGN { 1 0 10303 214 3 1 1 }'));
ENDSEC;

DATA;
#10=MECHANICAL_DESIGN_GEOMETRIC_PRESENTATION_REPRESENTATION('',(#322),#7835);
#238=ORIENTED_CLOSED_SHELL('',*,#4416,.F.);
#242=BREP_WITH_VOIDS('Body1',#4415,(#238));
#256=CONICAL_SURFACE('',#5126,0.475,0.785398163397449);
#257=CONICAL_SURFACE('',#5130,0.485,0.785398163397448);
#258=CONICAL_SURFACE('',#5134,0.31,0.463647609000806);
#259=CONICAL_SURFACE('',#5138,0.27,0.785398163397448);
#280=SHAPE_REPRESENTATION_RELATIONSHIP('SRR','None',#7970,#301);
#301=ADVANCED_BREP_SHAPE_REPRESENTATION('',(#242),#7834);
#322=STYLED_ITEM('',(#8151),#242);
#458=FACE_BOUND('',#1236,.T.);
#605=PLANE('',#5124);
#606=PLANE('',#5132);
#607=PLANE('',#5140);
#608=PLANE('',#5141);
#609=PLANE('',#5142);
#610=PLANE('',#5143);
#611=PLANE('',#5144);
#612=PLANE('',#5145);
#613=PLANE('',#5146);
#614=PLANE('',#5147);
#615=PLANE('',#5148);
#856=FACE_OUTER_BOUND('',#1231,.T.);
#857=FACE_OUTER_BOUND('',#1232,.T.);
#858=FACE_OUTER_BOUND('',#1233,.T.);
#859=FACE_OUTER_BOUND('',#1234,.T.);
#860=FACE_OUTER_BOUND('',#1235,.T.);
#861=FACE_OUTER_BOUND('',#1237,.T.);
#862=FACE_OUTER_BOUND('',#1238,.T.);
#863=FACE_OUTER_BOUND('',#1239,.T.);
#864=FACE_OUTER_BOUND('',#1240,.T.);
#865=FACE_OUTER_BOUND('',#1241,.T.);
#866=FACE_OUTER_BOUND('',#1242,.T.);
#867=FACE_OUTER_BOUND('',#1243,.T.);
#868=FACE_OUTER_BOUND('',#1244,.T.);
#869=FACE_OUTER_BOUND('',#1245,.T.);
#870=FACE_OUTER_BOUND('',#1246,.T.);
#871=FACE_OUTER_BOUND('',#1247,.T.);
#872=FACE_OUTER_BOUND('',#1248,.T.);
#1231=EDGE_LOOP('',(#3988));
#1232=EDGE_LOOP('',(#3989,#3990,#3991,#3992));
#1233=EDGE_LOOP('',(#3993,#3994,#3995,#3996));
#1234=EDGE_LOOP('',(#3997,#3998,#3999,#4000));
#1235=EDGE_LOOP('',(#4001));
#1236=EDGE_LOOP('',(#4002));
#1237=EDGE_LOOP('',(#4003,#4004,#4005,#4006));
#1238=EDGE_LOOP('',(#4007,#4008,#4009,#4010));
#1239=EDGE_LOOP('',(#4011,#4012,#4013,#4014));
#1240=EDGE_LOOP('',(#4015));
#1241=EDGE_LOOP('',(#4016,#4017,#4018,#4019));
#1242=EDGE_LOOP('',(#4020,#4021,#4022,#4023));
#1243=EDGE_LOOP('',(#4024,#4025,#4026,#4027));
#1244=EDGE_LOOP('',(#4028,#4029,#4030,#4031));
#1245=EDGE_LOOP('',(#4032,#4033,#4034,#4035));
#1246=EDGE_LOOP('',(#4036,#4037,#4038,#4039));
#1247=EDGE_LOOP('',(#4040,#4041,#4042,#4043,#4044,#4045));
#1248=EDGE_LOOP('',(#4046,#4047,#4048,#4049,#4050,#4051));
#1565=LINE('',#7694,#1905);
#1566=LINE('',#7698,#1906);
#1567=LINE('',#7702,#1907);
#1568=LINE('',#7709,#1908);
#1569=LINE('',#7713,#1909);
#1570=LINE('',#7717,#1910);
#1571=LINE('',#7722,#1911);
#1572=LINE('',#7724,#1912);
#1573=LINE('',#7726,#1913);
#1574=LINE('',#7727,#1914);
#1575=LINE('',#7730,#1915);
#1576=LINE('',#7732,#1916);
#1577=LINE('',#7733,#1917);
#1578=LINE('',#7736,#1918);
#1579=LINE('',#7738,#1919);
#1580=LINE('',#7739,#1920);
#1581=LINE('',#7742,#1921);
#1582=LINE('',#7744,#1922);
#1583=LINE('',#7745,#1923);
#1584=LINE('',#7748,#1924);
#1585=LINE('',#7750,#1925);
#1586=LINE('',#7751,#1926);
#1587=LINE('',#7753,#1927);
#1588=LINE('',#7754,#1928);
#1905=VECTOR('',#6450,0.475);
#1906=VECTOR('',#6455,0.5);
#1907=VECTOR('',#6460,0.485);
#1908=VECTOR('',#6469,0.31);
#1909=VECTOR('',#6474,0.3);
#1910=VECTOR('',#6479,0.27);
#1911=VECTOR('',#6484,1.);
#1912=VECTOR('',#6485,1.);
#1913=VECTOR('',#6486,1.);
#1914=VECTOR('',#6487,1.);
#1915=VECTOR('',#6490,1.);
#1916=VECTOR('',#6491,1.);
#1917=VECTOR('',#6492,1.);
#1918=VECTOR('',#6495,1.);
#1919=VECTOR('',#6496,1.);
#1920=VECTOR('',#6497,1.);
#1921=VECTOR('',#6500,1.);
#1922=VECTOR('',#6501,1.);
#1923=VECTOR('',#6502,1.);
#1924=VECTOR('',#6505,1.);
#1925=VECTOR('',#6506,1.);
#1926=VECTOR('',#6507,1.);
#1927=VECTOR('',#6510,1.);
#1928=VECTOR('',#6511,1.);
#2110=CIRCLE('',#5125,0.45);
#2111=CIRCLE('',#5127,0.5);
#2112=CIRCLE('',#5129,0.5);
#2113=CIRCLE('',#5131,0.47);
#2114=CIRCLE('',#5133,0.32);
#2115=CIRCLE('',#5135,0.2942);
#2116=CIRCLE('',#5137,0.2942);
#2117=CIRCLE('',#5139,0.24);
#2445=VERTEX_POINT('',#7689);
#2446=VERTEX_POINT('',#7692);
#2447=VERTEX_POINT('',#7696);
#2448=VERTEX_POINT('',#7700);
#2449=VERTEX_POINT('',#7704);
#2450=VERTEX_POINT('',#7707);
#2451=VERTEX_POINT('',#7711);
#2452=VERTEX_POINT('',#7715);
#2453=VERTEX_POINT('',#7720);
#2454=VERTEX_POINT('',#7721);
#2455=VERTEX_POINT('',#7723);
#2456=VERTEX_POINT('',#7725);
#2457=VERTEX_POINT('',#7729);
#2458=VERTEX_POINT('',#7731);
#2459=VERTEX_POINT('',#7735);
#2460=VERTEX_POINT('',#7737);
#2461=VERTEX_POINT('',#7741);
#2462=VERTEX_POINT('',#7743);
#2463=VERTEX_POINT('',#7747);
#2464=VERTEX_POINT('',#7749);
#2962=EDGE_CURVE('',#2445,#2445,#2110,.T.);
#2963=EDGE_CURVE('',#2446,#2446,#2111,.T.);
#2964=EDGE_CURVE('',#2446,#2445,#1565,.T.);
#2965=EDGE_CURVE('',#2447,#2447,#2112,.T.);
#2966=EDGE_CURVE('',#2447,#2446,#1566,.T.);
#2967=EDGE_CURVE('',#2448,#2448,#2113,.T.);
#2968=EDGE_CURVE('',#2448,#2447,#1567,.T.);
#2969=EDGE_CURVE('',#2449,#2449,#2114,.T.);
#2970=EDGE_CURVE('',#2450,#2450,#2115,.F.);
#2971=EDGE_CURVE('',#2450,#2449,#1568,.T.);
#2972=EDGE_CURVE('',#2451,#2451,#2116,.F.);
#2973=EDGE_CURVE('',#2451,#2450,#1569,.T.);
#2974=EDGE_CURVE('',#2452,#2452,#2117,.T.);
#2975=EDGE_CURVE('',#2452,#2451,#1570,.T.);
#2976=EDGE_CURVE('',#2453,#2454,#1571,.T.);
#2977=EDGE_CURVE('',#2454,#2455,#1572,.T.);
#2978=EDGE_CURVE('',#2455,#2456,#1573,.T.);
#2979=EDGE_CURVE('',#2453,#2456,#1574,.T.);
#2980=EDGE_CURVE('',#2454,#2457,#1575,.T.);
#2981=EDGE_CURVE('',#2457,#2458,#1576,.T.);
#2982=EDGE_CURVE('',#2458,#2455,#1577,.T.);
#2983=EDGE_CURVE('',#2457,#2459,#1578,.T.);
#2984=EDGE_CURVE('',#2459,#2460,#1579,.T.);
#2985=EDGE_CURVE('',#2460,#2458,#1580,.T.);
#2986=EDGE_CURVE('',#2459,#2461,#1581,.T.);
#2987=EDGE_CURVE('',#2461,#2462,#1582,.T.);
#2988=EDGE_CURVE('',#2462,#2460,#1583,.T.);
#2989=EDGE_CURVE('',#2461,#2463,#1584,.T.);
#2990=EDGE_CURVE('',#2463,#2464,#1585,.T.);
#2991=EDGE_CURVE('',#2464,#2462,#1586,.T.);
#2992=EDGE_CURVE('',#2463,#2453,#1587,.T.);
#2993=EDGE_CURVE('',#2456,#2464,#1588,.T.);
#3988=ORIENTED_EDGE('',*,*,#2962,.F.);
#3989=ORIENTED_EDGE('',*,*,#2963,.F.);
#3990=ORIENTED_EDGE('',*,*,#2964,.T.);
#3991=ORIENTED_EDGE('',*,*,#2962,.T.);
#3992=ORIENTED_EDGE('',*,*,#2964,.F.);
#3993=ORIENTED_EDGE('',*,*,#2965,.F.);
#3994=ORIENTED_EDGE('',*,*,#2966,.T.);
#3995=ORIENTED_EDGE('',*,*,#2963,.T.);
#3996=ORIENTED_EDGE('',*,*,#2966,.F.);
#3997=ORIENTED_EDGE('',*,*,#2967,.F.);
#3998=ORIENTED_EDGE('',*,*,#2968,.T.);
#3999=ORIENTED_EDGE('',*,*,#2965,.T.);
#4000=ORIENTED_EDGE('',*,*,#2968,.F.);
#4001=ORIENTED_EDGE('',*,*,#2967,.T.);
#4002=ORIENTED_EDGE('',*,*,#2969,.F.);
#4003=ORIENTED_EDGE('',*,*,#2970,.F.);
#4004=ORIENTED_EDGE('',*,*,#2971,.T.);
#4005=ORIENTED_EDGE('',*,*,#2969,.T.);
#4006=ORIENTED_EDGE('',*,*,#2971,.F.);
#4007=ORIENTED_EDGE('',*,*,#2972,.F.);
#4008=ORIENTED_EDGE('',*,*,#2973,.T.);
#4009=ORIENTED_EDGE('',*,*,#2970,.T.);
#4010=ORIENTED_EDGE('',*,*,#2973,.F.);
#4011=ORIENTED_EDGE('',*,*,#2974,.F.);
#4012=ORIENTED_EDGE('',*,*,#2975,.T.);
#4013=ORIENTED_EDGE('',*,*,#2972,.T.);
#4014=ORIENTED_EDGE('',*,*,#2975,.F.);
#4015=ORIENTED_EDGE('',*,*,#2974,.T.);
#4016=ORIENTED_EDGE('',*,*,#2976,.T.);
#4017=ORIENTED_EDGE('',*,*,#2977,.T.);
#4018=ORIENTED_EDGE('',*,*,#2978,.T.);
#4019=ORIENTED_EDGE('',*,*,#2979,.F.);
#4020=ORIENTED_EDGE('',*,*,#2980,.T.);
#4021=ORIENTED_EDGE('',*,*,#2981,.T.);
#4022=ORIENTED_EDGE('',*,*,#2982,.T.);
#4023=ORIENTED_EDGE('',*,*,#2977,.F.);
#4024=ORIENTED_EDGE('',*,*,#2983,.T.);
#4025=ORIENTED_EDGE('',*,*,#2984,.T.);
#4026=ORIENTED_EDGE('',*,*,#2985,.T.);
#4027=ORIENTED_EDGE('',*,*,#2981,.F.);
#4028=ORIENTED_EDGE('',*,*,#2986,.T.);
#4029=ORIENTED_EDGE('',*,*,#2987,.T.);
#4030=ORIENTED_EDGE('',*,*,#2988,.T.);
#4031=ORIENTED_EDGE('',*,*,#2984,.F.);
#4032=ORIENTED_EDGE('',*,*,#2989,.T.);
#4033=ORIENTED_EDGE('',*,*,#2990,.T.);
#4034=ORIENTED_EDGE('',*,*,#2991,.T.);
#4035=ORIENTED_EDGE('',*,*,#2987,.F.);
#4036=ORIENTED_EDGE('',*,*,#2992,.T.);
#4037=ORIENTED_EDGE('',*,*,#2979,.T.);
#4038=ORIENTED_EDGE('',*,*,#2993,.T.);
#4039=ORIENTED_EDGE('',*,*,#2990,.F.);
#4040=ORIENTED_EDGE('',*,*,#2992,.F.);
#4041=ORIENTED_EDGE('',*,*,#2989,.F.);
#4042=ORIENTED_EDGE('',*,*,#2986,.F.);
#4043=ORIENTED_EDGE('',*,*,#2983,.F.);
#4044=ORIENTED_EDGE('',*,*,#2980,.F.);
#4045=ORIENTED_EDGE('',*,*,#2976,.F.);
#4046=ORIENTED_EDGE('',*,*,#2993,.F.);
#4047=ORIENTED_EDGE('',*,*,#2978,.F.);
#4048=ORIENTED_EDGE('',*,*,#2982,.F.);
#4049=ORIENTED_EDGE('',*,*,#2985,.F.);
#4050=ORIENTED_EDGE('',*,*,#2988,.F.);
#4051=ORIENTED_EDGE('',*,*,#2991,.F.);
#4133=CYLINDRICAL_SURFACE('',#5128,0.5);
#4134=CYLINDRICAL_SURFACE('',#5136,0.2942);
#4375=ADVANCED_FACE('',(#856),#605,.T.);
#4376=ADVANCED_FACE('',(#857),#256,.T.);
#4377=ADVANCED_FACE('',(#858),#4133,.T.);
#4378=ADVANCED_FACE('',(#859),#257,.T.);
#4379=ADVANCED_FACE('',(#860,#458),#606,.T.);
#4380=ADVANCED_FACE('',(#861),#258,.T.);
#4381=ADVANCED_FACE('',(#862),#4134,.T.);
#4382=ADVANCED_FACE('',(#863),#259,.T.);
#4383=ADVANCED_FACE('',(#864),#607,.T.);
#4384=ADVANCED_FACE('',(#865),#608,.F.);
#4385=ADVANCED_FACE('',(#866),#609,.F.);
#4386=ADVANCED_FACE('',(#867),#610,.F.);
#4387=ADVANCED_FACE('',(#868),#611,.F.);
#4388=ADVANCED_FACE('',(#869),#612,.F.);
#4389=ADVANCED_FACE('',(#870),#613,.F.);
#4390=ADVANCED_FACE('',(#871),#614,.F.);
#4391=ADVANCED_FACE('',(#872),#615,.F.);
#4415=CLOSED_SHELL('',(#4375,#4376,#4377,#4378,#4379,#4380,#4381,#4382,
#4383));
#4416=CLOSED_SHELL('',(#4384,#4385,#4386,#4387,#4388,#4389,#4390,#4391));
#5123=AXIS2_PLACEMENT_3D('',#7687,#6440,#6441);
#5124=AXIS2_PLACEMENT_3D('',#7688,#6442,#6443);
#5125=AXIS2_PLACEMENT_3D('',#7690,#6444,#6445);
#5126=AXIS2_PLACEMENT_3D('',#7691,#6446,#6447);
#5127=AXIS2_PLACEMENT_3D('',#7693,#6448,#6449);
#5128=AXIS2_PLACEMENT_3D('',#7695,#6451,#6452);
#5129=AXIS2_PLACEMENT_3D('',#7697,#6453,#6454);
#5130=AXIS2_PLACEMENT_3D('',#7699,#6456,#6457);
#5131=AXIS2_PLACEMENT_3D('',#7701,#6458,#6459);
#5132=AXIS2_PLACEMENT_3D('',#7703,#6461,#6462);
#5133=AXIS2_PLACEMENT_3D('',#7705,#6463,#6464);
#5134=AXIS2_PLACEMENT_3D('',#7706,#6465,#6466);
#5135=AXIS2_PLACEMENT_3D('',#7708,#6467,#6468);
#5136=AXIS2_PLACEMENT_3D('',#7710,#6470,#6471);
#5137=AXIS2_PLACEMENT_3D('',#7712,#6472,#6473);
#5138=AXIS2_PLACEMENT_3D('',#7714,#6475,#6476);
#5139=AXIS2_PLACEMENT_3D('',#7716,#6477,#6478);
#5140=AXIS2_PLACEMENT_3D('',#7718,#6480,#6481);
#5141=AXIS2_PLACEMENT_3D('',#7719,#6482,#6483);
#5142=AXIS2_PLACEMENT_3D('',#7728,#6488,#6489);
#5143=AXIS2_PLACEMENT_3D('',#7734,#6493,#6494);
#5144=AXIS2_PLACEMENT_3D('',#7740,#6498,#6499);
#5145=AXIS2_PLACEMENT_3D('',#7746,#6503,#6504);
#5146=AXIS2_PLACEMENT_3D('',#7752,#6508,#6509);
#5147=AXIS2_PLACEMENT_3D('',#7755,#6512,#6513);
#5148=AXIS2_PLACEMENT_3D('',#7756,#6514,#6515);
#6440=DIRECTION('axis',(0.,0.,1.));
#6441=DIRECTION('refdir',(1.,0.,0.));
#6442=DIRECTION('center_axis',(0.,1.,0.));
#6443=DIRECTION('ref_axis',(0.,0.,1.));
#6444=DIRECTION('center_axis',(0.,-1.,0.));
#6445=DIRECTION('ref_axis',(1.,0.,0.));
#6446=DIRECTION('center_axis',(0.,-1.,0.));
#6447=DIRECTION('ref_axis',(1.,0.,0.));
#6448=DIRECTION('center_axis',(0.,-1.,0.));
#6449=DIRECTION('ref_axis',(1.,0.,0.));
#6450=DIRECTION('',(0.707106781186548,0.707106781186547,8.65956056235494E-17));
#6451=DIRECTION('center_axis',(0.,-1.,0.));
#6452=DIRECTION('ref_axis',(1.,0.,0.));
#6453=DIRECTION('center_axis',(0.,-1.,0.));
#6454=DIRECTION('ref_axis',(1.,0.,0.));
#6455=DIRECTION('',(0.,1.,0.));
#6456=DIRECTION('center_axis',(0.,1.,0.));
#6457=DIRECTION('ref_axis',(1.,0.,0.));
#6458=DIRECTION('center_axis',(0.,-1.,0.));
#6459=DIRECTION('ref_axis',(1.,0.,0.));
#6460=DIRECTION('',(-0.707106781186547,0.707106781186548,-8.65956056235493E-17));
#6461=DIRECTION('center_axis',(0.,-1.,0.));
#6462=DIRECTION('ref_axis',(0.,0.,-1.));
#6463=DIRECTION('center_axis',(0.,-1.,0.));
#6464=DIRECTION('ref_axis',(1.,0.,0.));
#6465=DIRECTION('center_axis',(0.,1.,0.));
#6466=DIRECTION('ref_axis',(1.,0.,0.));
#6467=DIRECTION('center_axis',(0.,1.,0.));
#6468=DIRECTION('ref_axis',(1.,0.,0.));
#6469=DIRECTION('',(-0.447213595499958,0.894427190999916,-5.47678698264203E-17));
#6470=DIRECTION('center_axis',(0.,-1.,0.));
#6471=DIRECTION('ref_axis',(1.,0.,0.));
#6472=DIRECTION('center_axis',(0.,1.,0.));
#6473=DIRECTION('ref_axis',(1.,0.,0.));
#6474=DIRECTION('',(0.,1.,0.));
#6475=DIRECTION('center_axis',(0.,1.,0.));
#6476=DIRECTION('ref_axis',(1.,0.,0.));
#6477=DIRECTION('center_axis',(0.,-1.,0.));
#6478=DIRECTION('ref_axis',(1.,0.,0.));
#6479=DIRECTION('',(-0.707106781186547,0.707106781186548,-8.65956056235493E-17));
#6480=DIRECTION('center_axis',(0.,-1.,0.));
#6481=DIRECTION('ref_axis',(0.,0.,-1.));
#6482=DIRECTION('center_axis',(0.866025403784439,0.,-0.5));
#6483=DIRECTION('ref_axis',(0.5,0.,0.866025403784439));
#6484=DIRECTION('',(-0.5,0.,-0.866025403784439));
#6485=DIRECTION('',(0.,-1.,0.));
#6486=DIRECTION('',(0.5,0.,0.866025403784439));
#6487=DIRECTION('',(0.,-1.,0.));
#6488=DIRECTION('center_axis',(1.92296268638356E-16,0.,-1.));
#6489=DIRECTION('ref_axis',(1.,0.,1.92296268638356E-16));
#6490=DIRECTION('',(-1.,0.,-1.92296268638356E-16));
#6491=DIRECTION('',(0.,-1.,0.));
#6492=DIRECTION('',(1.,0.,1.92296268638356E-16));
#6493=DIRECTION('center_axis',(-0.866025403784439,0.,-0.5));
#6494=DIRECTION('ref_axis',(0.5,0.,-0.866025403784439));
#6495=DIRECTION('',(-0.5,0.,0.866025403784438));
#6496=DIRECTION('',(0.,-1.,0.));
#6497=DIRECTION('',(0.5,0.,-0.866025403784438));
#6498=DIRECTION('center_axis',(-0.866025403784439,0.,0.5));
#6499=DIRECTION('ref_axis',(-0.5,0.,-0.866025403784439));
#6500=DIRECTION('',(0.5,0.,0.866025403784439));
#6501=DIRECTION('',(0.,-1.,0.));
#6502=DIRECTION('',(-0.5,0.,-0.866025403784439));
#6503=DIRECTION('center_axis',(-1.92296268638356E-16,0.,1.));
#6504=DIRECTION('ref_axis',(-1.,0.,-1.92296268638356E-16));
#6505=DIRECTION('',(1.,0.,1.92296268638356E-16));
#6506=DIRECTION('',(0.,-1.,0.));
#6507=DIRECTION('',(-1.,0.,-1.92296268638356E-16));
#6508=DIRECTION('center_axis',(0.866025403784439,0.,0.5));
#6509=DIRECTION('ref_axis',(-0.5,0.,0.866025403784439));
#6510=DIRECTION('',(0.5,0.,-0.866025403784439));
#6511=DIRECTION('',(-0.5,0.,0.866025403784439));
#6512=DIRECTION('center_axis',(0.,1.,0.));
#6513=DIRECTION('ref_axis',(1.,0.,0.));
#6514=DIRECTION('center_axis',(0.,-1.,0.));
#6515=DIRECTION('ref_axis',(0.,0.,-1.));
#7687=CARTESIAN_POINT('',(0.,0.,0.));
#7688=CARTESIAN_POINT('Origin',(0.45,0.6,0.));
#7689=CARTESIAN_POINT('',(-0.45,0.6,-5.51091059616309E-17));
#7690=CARTESIAN_POINT('Origin',(0.,0.6,0.));
#7691=CARTESIAN_POINT('Origin',(0.,0.575,0.));
#7692=CARTESIAN_POINT('',(-0.5,0.55,-6.12323399573677E-17));
#7693=CARTESIAN_POINT('Origin',(0.,0.55,0.));
#7694=CARTESIAN_POINT('',(-0.475,0.575,-5.81707229594993E-17));
#7695=CARTESIAN_POINT('Origin',(0.,0.29,0.));
#7696=CARTESIAN_POINT('',(-0.5,0.0299999999999998,-6.12323399573677E-17));
#7697=CARTESIAN_POINT('Origin',(0.,0.0299999999999998,0.));
#7698=CARTESIAN_POINT('',(-0.5,0.29,-6.12323399573677E-17));
#7699=CARTESIAN_POINT('Origin',(0.,0.0150000000000001,0.));
#7700=CARTESIAN_POINT('',(-0.47,7.11236625150491E-17,-5.75583995599256E-17));
#7701=CARTESIAN_POINT('Origin',(0.,0.,0.));
#7702=CARTESIAN_POINT('',(-0.485,0.0150000000000001,-5.93953697586466E-17));
#7703=CARTESIAN_POINT('Origin',(0.32,0.,0.));
#7704=CARTESIAN_POINT('',(-0.32,-6.93889390390723E-18,-3.91886975727153E-17));
#7705=CARTESIAN_POINT('Origin',(0.,0.,0.));
#7706=CARTESIAN_POINT('Origin',(0.,-0.02,0.));
#7707=CARTESIAN_POINT('',(-0.2942,-0.0515999999999999,3.60291088309151E-17));
#7708=CARTESIAN_POINT('Origin',(0.,-0.0515999999999999,0.));
#7709=CARTESIAN_POINT('',(-0.31,-0.02,-3.7964050773568E-17));
#7710=CARTESIAN_POINT('Origin',(0.,-1.24,0.));
#7711=CARTESIAN_POINT('',(-0.2942,-2.4458,3.60291088309151E-17));
#7712=CARTESIAN_POINT('Origin',(0.,-2.4458,0.));
#7713=CARTESIAN_POINT('',(-0.2942,-1.24,-3.60291088309151E-17));
#7714=CARTESIAN_POINT('Origin',(0.,-2.47,0.));
#7715=CARTESIAN_POINT('',(-0.24,-2.5,-2.93915231795365E-17));
#7716=CARTESIAN_POINT('Origin',(0.,-2.5,0.));
#7717=CARTESIAN_POINT('',(-0.27,-2.47,-3.30654635769785E-17));
#7718=CARTESIAN_POINT('Origin',(0.,-2.5,0.));
#7719=CARTESIAN_POINT('Origin',(0.144337567297406,-0.6,-0.25));
#7720=CARTESIAN_POINT('',(0.288675134594813,-0.6,0.));
#7721=CARTESIAN_POINT('',(0.144337567297406,-0.6,-0.25));
#7722=CARTESIAN_POINT('',(0.288675134594813,-0.6,0.));
#7723=CARTESIAN_POINT('',(0.144337567297406,-0.96,-0.25));
#7724=CARTESIAN_POINT('',(0.144337567297406,-0.6,-0.25));
#7725=CARTESIAN_POINT('',(0.288675134594813,-0.96,0.));
#7726=CARTESIAN_POINT('',(0.288675134594813,-0.96,0.));
#7727=CARTESIAN_POINT('',(0.288675134594813,-0.6,0.));
#7728=CARTESIAN_POINT('Origin',(-0.144337567297406,-0.6,-0.25));
#7729=CARTESIAN_POINT('',(-0.144337567297406,-0.6,-0.25));
#7730=CARTESIAN_POINT('',(0.144337567297406,-0.6,-0.25));
#7731=CARTESIAN_POINT('',(-0.144337567297406,-0.96,-0.25));
#7732=CARTESIAN_POINT('',(-0.144337567297406,-0.6,-0.25));
#7733=CARTESIAN_POINT('',(0.144337567297406,-0.96,-0.25));
#7734=CARTESIAN_POINT('Origin',(-0.288675134594813,-0.6,-8.32667268468867E-17));
#7735=CARTESIAN_POINT('',(-0.288675134594813,-0.6,-3.53525079574969E-17));
#7736=CARTESIAN_POINT('',(-0.144337567297406,-0.6,-0.25));
#7737=CARTESIAN_POINT('',(-0.288675134594813,-0.96,-5.55111512312578E-17));
#7738=CARTESIAN_POINT('',(-0.288675134594813,-0.6,-3.53525079574969E-17));
#7739=CARTESIAN_POINT('',(-0.144337567297406,-0.96,-0.25));
#7740=CARTESIAN_POINT('Origin',(-0.144337567297407,-0.6,0.25));
#7741=CARTESIAN_POINT('',(-0.144337567297407,-0.6,0.25));
#7742=CARTESIAN_POINT('',(-0.288675134594813,-0.6,-3.53525079574969E-17));
#7743=CARTESIAN_POINT('',(-0.144337567297407,-0.96,0.25));
#7744=CARTESIAN_POINT('',(-0.144337567297407,-0.6,0.25));
#7745=CARTESIAN_POINT('',(-0.288675134594813,-0.96,-3.53525079574969E-17));
#7746=CARTESIAN_POINT('Origin',(0.144337567297406,-0.6,0.25));
#7747=CARTESIAN_POINT('',(0.144337567297406,-0.6,0.25));
#7748=CARTESIAN_POINT('',(-0.144337567297407,-0.6,0.25));
#7749=CARTESIAN_POINT('',(0.144337567297406,-0.96,0.25));
#7750=CARTESIAN_POINT('',(0.144337567297406,-0.6,0.25));
#7751=CARTESIAN_POINT('',(-0.144337567297407,-0.96,0.25));
#7752=CARTESIAN_POINT('Origin',(0.288675134594813,-0.6,0.));
#7753=CARTESIAN_POINT('',(0.144337567297406,-0.6,0.25));
#7754=CARTESIAN_POINT('',(0.144337567297406,-0.96,0.25));
#7755=CARTESIAN_POINT('Origin',(0.,-0.6,0.));
#7756=CARTESIAN_POINT('Origin',(0.,-0.96,0.));
#7808=UNCERTAINTY_MEASURE_WITH_UNIT(LENGTH_MEASURE(0.001),#7836,
'DISTANCE_ACCURACY_VALUE',
'Maximum model space distance between geometric entities at asserted c
onnectivities');
#7809=UNCERTAINTY_MEASURE_WITH_UNIT(LENGTH_MEASURE(0.001),#7836,
'DISTANCE_ACCURACY_VALUE',
'Maximum model space distance between geometric entities at asserted c
onnectivities');
#7834=(
GEOMETRIC_REPRESENTATION_CONTEXT(3)
GLOBAL_UNCERTAINTY_ASSIGNED_CONTEXT((#7808))
GLOBAL_UNIT_ASSIGNED_CONTEXT((#7836,#7838,#7839))
REPRESENTATION_CONTEXT('','3D')
);
#7835=(
GEOMETRIC_REPRESENTATION_CONTEXT(3)
GLOBAL_UNCERTAINTY_ASSIGNED_CONTEXT((#7809))
GLOBAL_UNIT_ASSIGNED_CONTEXT((#7836,#7838,#7839))
REPRESENTATION_CONTEXT('','3D')
);
#7836=(
LENGTH_UNIT()
NAMED_UNIT(*)
SI_UNIT(.CENTI.,.METRE.)
);
#7838=(
NAMED_UNIT(*)
PLANE_ANGLE_UNIT()
SI_UNIT($,.RADIAN.)
);
#7839=(
NAMED_UNIT(*)
SI_UNIT($,.STERADIAN.)
SOLID_ANGLE_UNIT()
);
#7864=SHAPE_DEFINITION_REPRESENTATION(#7918,#7970);
#7918=PRODUCT_DEFINITION_SHAPE('',$,#7996);
#7970=SHAPE_REPRESENTATION('',(#5123),#7834);
#7971=PRODUCT_DEFINITION_CONTEXT('part definition',#8048,'design');
#7996=PRODUCT_DEFINITION('Cap Screw - M6x25','Cap Screw - M6x25',#8021,
#7971);
#8021=PRODUCT_DEFINITION_FORMATION('',$,#8074);
#8048=APPLICATION_CONTEXT(
'Core Data for Automotive Mechanical Design Process');
#8049=PRODUCT_CONTEXT('part definition',#8048,'mechanical');
#8074=PRODUCT('Cap Screw - M6x25','Cap Screw - M6x25',
'Cap Screw - M6x25',(#8049));
#8145=COLOUR_RGB('Black',0.12,0.14,0.17);
#8146=FILL_AREA_STYLE_COLOUR('',#8145);
#8147=FILL_AREA_STYLE('',(#8146));
#8148=SURFACE_STYLE_FILL_AREA(#8147);
#8149=SURFACE_SIDE_STYLE('',(#8148));
#8150=SURFACE_STYLE_USAGE(.BOTH.,#8149);
#8151=PRESENTATION_STYLE_ASSIGNMENT((#8150));
ENDSEC;
END-ISO-10303-21;
